ISO-10303-21;
HEADER;
/* Generated by software containing ST-Developer
 * from STEP Tools, Inc. (www.steptools.com) 
 */

FILE_DESCRIPTION(
/* description */ ('PAT-097'),
/* implementation_level */ '2;1');

FILE_NAME(
/* name */ 'Hex Nut - M8.step',
/* time_stamp */ '2026-10-29T15:59:31-07:00',
/* author */ (''),
/* organization */ (''),
/* preprocessor_version */ 'ST-DEVELOPER v20.2',
/* originating_system */ 'Autodesk Translation Framework v15.17.0.0',
/* authorisation */ '');

FILE_SCHEMA (('AUTOMOTIVE_DESIGN { 1 0 10303 214 3 1 1 }'));
ENDSEC;

DATA;
#10=MECHANICAL_DESIGN_GEOMETRIC_PRESENTATION_REPRESENTATION('',(#81),#2768);
#47=(
BOUNDED_CURVE()
B_SPLINE_CURVE(2,(#2669,#2670,#2671),.UNSPECIFIED.,.F.,.F.)
B_SPLINE_CURVE_WITH_KNOTS((3,3),(0.14973948338295,0.97160236658079),
 .UNSPECIFIED.)
CURVE()
GEOMETRIC_REPRESENTATION_ITEM()
RATIONAL_B_SPLINE_CURVE((1.07140024848292,1.23714644374248,1.07140024848292))
REPRESENTATION_ITEM('')
);
#48=(
BOUNDED_CURVE()
B_SPLINE_CURVE(2,(#2673,#2674,#2675),.UNSPECIFIED.,.F.,.F.)
B_SPLINE_CURVE_WITH_KNOTS((3,3),(0.14973948338295,0.971602366580789),
 .UNSPECIFIED.)
CURVE()
GEOMETRIC_REPRESENTATION_ITEM()
RATIONAL_B_SPLINE_CURVE((1.07140024848292,1.23714644374248,1.07140024848292))
REPRESENTATION_ITEM('')
);
#49=(
BOUNDED_CURVE()
B_SPLINE_CURVE(2,(#2680,#2681,#2682),.UNSPECIFIED.,.F.,.F.)
B_SPLINE_CURVE_WITH_KNOTS((3,3),(0.14973948338295,0.97160236658079),
 .UNSPECIFIED.)
CURVE()
GEOMETRIC_REPRESENTATION_ITEM()
RATIONAL_B_SPLINE_CURVE((1.07140024848292,1.23714644374248,1.07140024848292))
REPRESENTATION_ITEM('')
);
#50=(
BOUNDED_CURVE()
B_SPLINE_CURVE(2,(#2684,#2685,#2686),.UNSPECIFIED.,.F.,.F.)
B_SPLINE_CURVE_WITH_KNOTS((3,3),(0.14973948338295,0.97160236658079),
 .UNSPECIFIED.)
CURVE()
GEOMETRIC_REPRESENTATION_ITEM()
RATIONAL_B_SPLINE_CURVE((1.07140024848292,1.23714644374248,1.07140024848292))
REPRESENTATION_ITEM('')
);
#51=(
BOUNDED_CURVE()
B_SPLINE_CURVE(2,(#2688,#2689,#2690),.UNSPECIFIED.,.F.,.F.)
B_SPLINE_CURVE_WITH_KNOTS((3,3),(0.14973948338295,0.971602366580789),
 .UNSPECIFIED.)
CURVE()
GEOMETRIC_REPRESENTATION_ITEM()
RATIONAL_B_SPLINE_CURVE((1.07140024848292,1.23714644374248,1.07140024848292))
REPRESENTATION_ITEM('')
);
#52=(
BOUNDED_CURVE()
B_SPLINE_CURVE(2,(#2691,#2692,#2693),.UNSPECIFIED.,.F.,.F.)
B_SPLINE_CURVE_WITH_KNOTS((3,3),(0.14973948338295,0.97160236658079),
 .UNSPECIFIED.)
CURVE()
GEOMETRIC_REPRESENTATION_ITEM()
RATIONAL_B_SPLINE_CURVE((1.07140024848292,1.23714644374248,1.07140024848292))
REPRESENTATION_ITEM('')
);
#53=(
BOUNDED_CURVE()
B_SPLINE_CURVE(2,(#2700,#2701,#2702),.UNSPECIFIED.,.F.,.F.)
B_SPLINE_CURVE_WITH_KNOTS((3,3),(0.14973948338295,0.97160236658079),
 .UNSPECIFIED.)
CURVE()
GEOMETRIC_REPRESENTATION_ITEM()
RATIONAL_B_SPLINE_CURVE((1.07140024848292,1.23714644374248,1.07140024848292))
REPRESENTATION_ITEM('')
);
#54=(
BOUNDED_CURVE()
B_SPLINE_CURVE(2,(#2704,#2705,#2706),.UNSPECIFIED.,.F.,.F.)
B_SPLINE_CURVE_WITH_KNOTS((3,3),(0.14973948338295,0.97160236658079),
 .UNSPECIFIED.)
CURVE()
GEOMETRIC_REPRESENTATION_ITEM()
RATIONAL_B_SPLINE_CURVE((1.07140024848292,1.23714644374248,1.07140024848292))
REPRESENTATION_ITEM('')
);
#55=(
BOUNDED_CURVE()
B_SPLINE_CURVE(2,(#2708,#2709,#2710),.UNSPECIFIED.,.F.,.F.)
B_SPLINE_CURVE_WITH_KNOTS((3,3),(0.14973948338295,0.971602366580789),
 .UNSPECIFIED.)
CURVE()
GEOMETRIC_REPRESENTATION_ITEM()
RATIONAL_B_SPLINE_CURVE((1.07140024848292,1.23714644374248,1.07140024848292))
REPRESENTATION_ITEM('')
);
#56=(
BOUNDED_CURVE()
B_SPLINE_CURVE(2,(#2712,#2713,#2714),.UNSPECIFIED.,.F.,.F.)
B_SPLINE_CURVE_WITH_KNOTS((3,3),(0.14973948338295,0.97160236658079),
 .UNSPECIFIED.)
CURVE()
GEOMETRIC_REPRESENTATION_ITEM()
RATIONAL_B_SPLINE_CURVE((1.07140024848292,1.23714644374248,1.07140024848292))
REPRESENTATION_ITEM('')
);
#57=(
BOUNDED_CURVE()
B_SPLINE_CURVE(2,(#2716,#2717,#2718),.UNSPECIFIED.,.F.,.F.)
B_SPLINE_CURVE_WITH_KNOTS((3,3),(0.14973948338295,0.97160236658079),
 .UNSPECIFIED.)
CURVE()
GEOMETRIC_REPRESENTATION_ITEM()
RATIONAL_B_SPLINE_CURVE((1.07140024848292,1.23714644374248,1.07140024848292))
REPRESENTATION_ITEM('')
);
#58=(
BOUNDED_CURVE()
B_SPLINE_CURVE(2,(#2719,#2720,#2721),.UNSPECIFIED.,.F.,.F.)
B_SPLINE_CURVE_WITH_KNOTS((3,3),(0.14973948338295,0.971602366580789),
 .UNSPECIFIED.)
CURVE()
GEOMETRIC_REPRESENTATION_ITEM()
RATIONAL_B_SPLINE_CURVE((1.07140024848292,1.23714644374248,1.07140024848292))
REPRESENTATION_ITEM('')
);
#59=CONICAL_SURFACE('',#1813,0.734027674973257,1.0471975511966);
#60=CONICAL_SURFACE('',#1815,0.734027674973257,1.0471975511966);
#67=SHAPE_REPRESENTATION_RELATIONSHIP('SRR','None',#2805,#74);
#74=ADVANCED_BREP_SHAPE_REPRESENTATION('',(#88),#2767);
#81=STYLED_ITEM('',(#2918),#88);
#88=MANIFOLD_SOLID_BREP('Body1',#1602);
#115=CYLINDRICAL_SURFACE('',#1820,0.338975);
#162=FACE_BOUND('',#431,.T.);
#163=FACE_BOUND('',#433,.T.);
#216=CIRCLE('',#1814,0.6175);
#217=CIRCLE('',#1816,0.6175);
#218=CIRCLE('',#1821,0.338975);
#219=CIRCLE('',#1822,0.338975);
#292=FACE_OUTER_BOUND('',#421,.T.);
#293=FACE_OUTER_BOUND('',#422,.T.);
#294=FACE_OUTER_BOUND('',#423,.T.);
#295=FACE_OUTER_BOUND('',#424,.T.);
#296=FACE_OUTER_BOUND('',#425,.T.);
#297=FACE_OUTER_BOUND('',#426,.T.);
#298=FACE_OUTER_BOUND('',#427,.T.);
#299=FACE_OUTER_BOUND('',#428,.T.);
#300=FACE_OUTER_BOUND('',#429,.T.);
#301=FACE_OUTER_BOUND('',#430,.T.);
#302=FACE_OUTER_BOUND('',#432,.T.);
#421=EDGE_LOOP('',(#1409,#1410,#1411,#1412,#1413,#1414,#1415,#1416,#1417));
#422=EDGE_LOOP('',(#1418,#1419,#1420,#1421,#1422,#1423,#1424,#1425,#1426));
#423=EDGE_LOOP('',(#1427,#1428,#1429,#1430));
#424=EDGE_LOOP('',(#1431,#1432,#1433,#1434));
#425=EDGE_LOOP('',(#1435,#1436,#1437,#1438));
#426=EDGE_LOOP('',(#1439,#1440,#1441,#1442));
#427=EDGE_LOOP('',(#1443,#1444,#1445,#1446));
#428=EDGE_LOOP('',(#1447,#1448,#1449,#1450));
#429=EDGE_LOOP('',(#1451,#1452,#1453,#1454));
#430=EDGE_LOOP('',(#1455));
#431=EDGE_LOOP('',(#1456));
#432=EDGE_LOOP('',(#1457));
#433=EDGE_LOOP('',(#1458));
#562=LINE('',#2677,#699);
#563=LINE('',#2698,#700);
#564=LINE('',#2723,#701);
#565=LINE('',#2724,#702);
#566=LINE('',#2726,#703);
#567=LINE('',#2728,#704);
#568=LINE('',#2733,#705);
#569=LINE('',#2736,#706);
#570=LINE('',#2738,#707);
#699=VECTOR('',#2231,0.734027674973257);
#700=VECTOR('',#2238,0.734027674973257);
#701=VECTOR('',#2241,1.);
#702=VECTOR('',#2242,1.);
#703=VECTOR('',#2245,1.);
#704=VECTOR('',#2248,1.);
#705=VECTOR('',#2253,0.4);
#706=VECTOR('',#2258,1.);
#707=VECTOR('',#2261,1.);
#828=VERTEX_POINT('',#2667);
#829=VERTEX_POINT('',#2668);
#830=VERTEX_POINT('',#2672);
#831=VERTEX_POINT('',#2676);
#832=VERTEX_POINT('',#2679);
#833=VERTEX_POINT('',#2683);
#834=VERTEX_POINT('',#2687);
#835=VERTEX_POINT('',#2695);
#836=VERTEX_POINT('',#2697);
#837=VERTEX_POINT('',#2699);
#838=VERTEX_POINT('',#2703);
#839=VERTEX_POINT('',#2707);
#840=VERTEX_POINT('',#2711);
#841=VERTEX_POINT('',#2715);
#842=VERTEX_POINT('',#2730);
#843=VERTEX_POINT('',#2732);
#1024=EDGE_CURVE('',#828,#829,#47,.T.);
#1025=EDGE_CURVE('',#830,#828,#48,.T.);
#1026=EDGE_CURVE('',#830,#831,#562,.T.);
#1027=EDGE_CURVE('',#831,#831,#216,.T.);
#1028=EDGE_CURVE('',#832,#830,#49,.T.);
#1029=EDGE_CURVE('',#833,#832,#50,.T.);
#1030=EDGE_CURVE('',#834,#833,#51,.T.);
#1031=EDGE_CURVE('',#829,#834,#52,.T.);
#1032=EDGE_CURVE('',#835,#835,#217,.T.);
#1033=EDGE_CURVE('',#835,#836,#563,.T.);
#1034=EDGE_CURVE('',#837,#836,#53,.T.);
#1035=EDGE_CURVE('',#838,#837,#54,.T.);
#1036=EDGE_CURVE('',#839,#838,#55,.T.);
#1037=EDGE_CURVE('',#840,#839,#56,.T.);
#1038=EDGE_CURVE('',#841,#840,#57,.T.);
#1039=EDGE_CURVE('',#836,#841,#58,.T.);
#1040=EDGE_CURVE('',#832,#841,#564,.T.);
#1041=EDGE_CURVE('',#833,#840,#565,.T.);
#1042=EDGE_CURVE('',#830,#836,#566,.T.);
#1043=EDGE_CURVE('',#828,#837,#567,.T.);
#1044=EDGE_CURVE('',#842,#842,#218,.F.);
#1045=EDGE_CURVE('',#842,#843,#568,.T.);
#1046=EDGE_CURVE('',#843,#843,#219,.F.);
#1047=EDGE_CURVE('',#829,#838,#569,.T.);
#1048=EDGE_CURVE('',#834,#839,#570,.T.);
#1409=ORIENTED_EDGE('',*,*,#1024,.F.);
#1410=ORIENTED_EDGE('',*,*,#1025,.F.);
#1411=ORIENTED_EDGE('',*,*,#1026,.T.);
#1412=ORIENTED_EDGE('',*,*,#1027,.F.);
#1413=ORIENTED_EDGE('',*,*,#1026,.F.);
#1414=ORIENTED_EDGE('',*,*,#1028,.F.);
#1415=ORIENTED_EDGE('',*,*,#1029,.F.);
#1416=ORIENTED_EDGE('',*,*,#1030,.F.);
#1417=ORIENTED_EDGE('',*,*,#1031,.F.);
#1418=ORIENTED_EDGE('',*,*,#1032,.F.);
#1419=ORIENTED_EDGE('',*,*,#1033,.T.);
#1420=ORIENTED_EDGE('',*,*,#1034,.F.);
#1421=ORIENTED_EDGE('',*,*,#1035,.F.);
#1422=ORIENTED_EDGE('',*,*,#1036,.F.);
#1423=ORIENTED_EDGE('',*,*,#1037,.F.);
#1424=ORIENTED_EDGE('',*,*,#1038,.F.);
#1425=ORIENTED_EDGE('',*,*,#1039,.F.);
#1426=ORIENTED_EDGE('',*,*,#1033,.F.);
#1427=ORIENTED_EDGE('',*,*,#1029,.T.);
#1428=ORIENTED_EDGE('',*,*,#1040,.T.);
#1429=ORIENTED_EDGE('',*,*,#1038,.T.);
#1430=ORIENTED_EDGE('',*,*,#1041,.F.);
#1431=ORIENTED_EDGE('',*,*,#1028,.T.);
#1432=ORIENTED_EDGE('',*,*,#1042,.T.);
#1433=ORIENTED_EDGE('',*,*,#1039,.T.);
#1434=ORIENTED_EDGE('',*,*,#1040,.F.);
#1435=ORIENTED_EDGE('',*,*,#1025,.T.);
#1436=ORIENTED_EDGE('',*,*,#1043,.T.);
#1437=ORIENTED_EDGE('',*,*,#1034,.T.);
#1438=ORIENTED_EDGE('',*,*,#1042,.F.);
#1439=ORIENTED_EDGE('',*,*,#1044,.F.);
#1440=ORIENTED_EDGE('',*,*,#1045,.T.);
#1441=ORIENTED_EDGE('',*,*,#1046,.T.);
#1442=ORIENTED_EDGE('',*,*,#1045,.F.);
#1443=ORIENTED_EDGE('',*,*,#1024,.T.);
#1444=ORIENTED_EDGE('',*,*,#1047,.T.);
#1445=ORIENTED_EDGE('',*,*,#1035,.T.);
#1446=ORIENTED_EDGE('',*,*,#1043,.F.);
#1447=ORIENTED_EDGE('',*,*,#1030,.T.);
#1448=ORIENTED_EDGE('',*,*,#1041,.T.);
#1449=ORIENTED_EDGE('',*,*,#1037,.T.);
#1450=ORIENTED_EDGE('',*,*,#1048,.F.);
#1451=ORIENTED_EDGE('',*,*,#1031,.T.);
#1452=ORIENTED_EDGE('',*,*,#1048,.T.);
#1453=ORIENTED_EDGE('',*,*,#1036,.T.);
#1454=ORIENTED_EDGE('',*,*,#1047,.F.);
#1455=ORIENTED_EDGE('',*,*,#1032,.T.);
#1456=ORIENTED_EDGE('',*,*,#1044,.T.);
#1457=ORIENTED_EDGE('',*,*,#1027,.T.);
#1458=ORIENTED_EDGE('',*,*,#1046,.F.);
#1505=PLANE('',#1817);
#1506=PLANE('',#1818);
#1507=PLANE('',#1819);
#1508=PLANE('',#1823);
#1509=PLANE('',#1824);
#1510=PLANE('',#1825);
#1511=PLANE('',#1826);
#1512=PLANE('',#1827);
#1585=ADVANCED_FACE('',(#292),#59,.T.);
#1586=ADVANCED_FACE('',(#293),#60,.T.);
#1587=ADVANCED_FACE('',(#294),#1505,.T.);
#1588=ADVANCED_FACE('',(#295),#1506,.T.);
#1589=ADVANCED_FACE('',(#296),#1507,.T.);
#1590=ADVANCED_FACE('',(#297),#115,.F.);
#1591=ADVANCED_FACE('',(#298),#1508,.T.);
#1592=ADVANCED_FACE('',(#299),#1509,.T.);
#1593=ADVANCED_FACE('',(#300),#1510,.T.);
#1594=ADVANCED_FACE('',(#301,#162),#1511,.T.);
#1595=ADVANCED_FACE('',(#302,#163),#1512,.F.);
#1602=CLOSED_SHELL('',(#1585,#1586,#1587,#1588,#1589,#1590,#1591,#1592,
#1593,#1594,#1595));
#1812=AXIS2_PLACEMENT_3D('',#2665,#2227,#2228);
#1813=AXIS2_PLACEMENT_3D('',#2666,#2229,#2230);
#1814=AXIS2_PLACEMENT_3D('',#2678,#2232,#2233);
#1815=AXIS2_PLACEMENT_3D('',#2694,#2234,#2235);
#1816=AXIS2_PLACEMENT_3D('',#2696,#2236,#2237);
#1817=AXIS2_PLACEMENT_3D('',#2722,#2239,#2240);
#1818=AXIS2_PLACEMENT_3D('',#2725,#2243,#2244);
#1819=AXIS2_PLACEMENT_3D('',#2727,#2246,#2247);
#1820=AXIS2_PLACEMENT_3D('',#2729,#2249,#2250);
#1821=AXIS2_PLACEMENT_3D('',#2731,#2251,#2252);
#1822=AXIS2_PLACEMENT_3D('',#2734,#2254,#2255);
#1823=AXIS2_PLACEMENT_3D('',#2735,#2256,#2257);
#1824=AXIS2_PLACEMENT_3D('',#2737,#2259,#2260);
#1825=AXIS2_PLACEMENT_3D('',#2739,#2262,#2263);
#1826=AXIS2_PLACEMENT_3D('',#2740,#2264,#2265);
#1827=AXIS2_PLACEMENT_3D('',#2741,#2266,#2267);
#2227=DIRECTION('axis',(0.,0.,1.));
#2228=DIRECTION('refdir',(1.,0.,0.));
#2229=DIRECTION('center_axis',(0.,1.,0.));
#2230=DIRECTION('ref_axis',(1.,0.,0.));
#2231=DIRECTION('',(0.866025403784439,-0.5,1.06057523872491E-16));
#2232=DIRECTION('center_axis',(0.,-1.,0.));
#2233=DIRECTION('ref_axis',(1.,0.,0.));
#2234=DIRECTION('center_axis',(0.,-1.,0.));
#2235=DIRECTION('ref_axis',(1.,0.,0.));
#2236=DIRECTION('center_axis',(0.,1.,0.));
#2237=DIRECTION('ref_axis',(1.,0.,0.));
#2238=DIRECTION('',(-0.866025403784439,-0.5,-1.06057523872491E-16));
#2239=DIRECTION('center_axis',(1.4792020664489E-16,0.,-1.));
#2240=DIRECTION('ref_axis',(-1.,0.,-1.4792020664489E-16));
#2241=DIRECTION('',(0.,1.,0.));
#2242=DIRECTION('',(0.,1.,0.));
#2243=DIRECTION('center_axis',(-0.866025403784439,0.,-0.5));
#2244=DIRECTION('ref_axis',(-0.5,0.,0.866025403784439));
#2245=DIRECTION('',(0.,1.,0.));
#2246=DIRECTION('center_axis',(-0.866025403784439,0.,0.5));
#2247=DIRECTION('ref_axis',(0.5,0.,0.866025403784439));
#2248=DIRECTION('',(0.,1.,0.));
#2249=DIRECTION('center_axis',(0.,1.,0.));
#2250=DIRECTION('ref_axis',(1.,0.,0.));
#2251=DIRECTION('center_axis',(0.,1.,0.));
#2252=DIRECTION('ref_axis',(1.,0.,0.));
#2253=DIRECTION('',(0.,-1.,0.));
#2254=DIRECTION('center_axis',(0.,1.,0.));
#2255=DIRECTION('ref_axis',(1.,0.,0.));
#2256=DIRECTION('center_axis',(-2.95840413289779E-16,0.,1.));
#2257=DIRECTION('ref_axis',(1.,0.,2.95840413289779E-16));
#2258=DIRECTION('',(0.,1.,0.));
#2259=DIRECTION('center_axis',(0.866025403784439,0.,-0.5));
#2260=DIRECTION('ref_axis',(-0.5,0.,-0.866025403784439));
#2261=DIRECTION('',(0.,1.,0.));
#2262=DIRECTION('center_axis',(0.866025403784439,0.,0.5));
#2263=DIRECTION('ref_axis',(0.5,0.,-0.866025403784439));
#2264=DIRECTION('center_axis',(0.,1.,0.));
#2265=DIRECTION('ref_axis',(1.,0.,0.));
#2266=DIRECTION('center_axis',(0.,1.,0.));
#2267=DIRECTION('ref_axis',(1.,0.,0.));
#2665=CARTESIAN_POINT('',(0.,0.,0.));
#2666=CARTESIAN_POINT('Origin',(0.,0.067277284513851,0.));
#2667=CARTESIAN_POINT('',(-0.375277674973257,0.0768195421087395,0.65));
#2668=CARTESIAN_POINT('',(0.375277674973257,0.0768195421087395,0.65));
#2669=CARTESIAN_POINT('Ctrl Pts',(-0.375277674973257,0.0768195421087395,
0.65));
#2670=CARTESIAN_POINT('Ctrl Pts',(1.66533453693773E-13,-0.0315137912242439,
0.65));
#2671=CARTESIAN_POINT('Ctrl Pts',(0.375277674973257,0.0768195421087394,
0.65));
#2672=CARTESIAN_POINT('',(-0.750555349946514,0.0768195421087394,-9.19165206894919E-17));
#2673=CARTESIAN_POINT('Ctrl Pts',(-0.750555349946514,0.0768195421087394,
-9.19165206894919E-17));
#2674=CARTESIAN_POINT('Ctrl Pts',(-0.562916512459802,-0.0315137912242434,
0.325000000000144));
#2675=CARTESIAN_POINT('Ctrl Pts',(-0.375277674973257,0.0768195421087395,
0.65));
#2676=CARTESIAN_POINT('',(-0.6175,-2.77555756156289E-17,-7.5621939847349E-17));
#2677=CARTESIAN_POINT('',(-0.734027674973257,0.067277284513851,-8.98924642641573E-17));
#2678=CARTESIAN_POINT('Origin',(0.,0.,0.));
#2679=CARTESIAN_POINT('',(-0.375277674973257,0.0768195421087395,-0.65));
#2680=CARTESIAN_POINT('Ctrl Pts',(-0.375277674973257,0.0768195421087395,
-0.65));
#2681=CARTESIAN_POINT('Ctrl Pts',(-0.562916512459968,-0.0315137912242437,
-0.324999999999856));
#2682=CARTESIAN_POINT('Ctrl Pts',(-0.750555349946514,0.0768195421087395,
-9.19165206894919E-17));
#2683=CARTESIAN_POINT('',(0.375277674973257,0.0768195421087395,-0.65));
#2684=CARTESIAN_POINT('Ctrl Pts',(0.375277674973257,0.0768195421087395,
-0.65));
#2685=CARTESIAN_POINT('Ctrl Pts',(-1.66144875635155E-13,-0.0315137912242437,
-0.65));
#2686=CARTESIAN_POINT('Ctrl Pts',(-0.375277674973257,0.0768195421087395,
-0.65));
#2687=CARTESIAN_POINT('',(0.750555349946514,0.0768195421087394,0.));
#2688=CARTESIAN_POINT('Ctrl Pts',(0.750555349946514,0.0768195421087394,
0.));
#2689=CARTESIAN_POINT('Ctrl Pts',(0.562916512459802,-0.0315137912242436,
-0.325000000000144));
#2690=CARTESIAN_POINT('Ctrl Pts',(0.375277674973257,0.0768195421087395,
-0.65));
#2691=CARTESIAN_POINT('Ctrl Pts',(0.375277674973257,0.0768195421087394,
0.65));
#2692=CARTESIAN_POINT('Ctrl Pts',(0.562916512459968,-0.0315137912242439,
0.324999999999856));
#2693=CARTESIAN_POINT('Ctrl Pts',(0.750555349946514,0.0768195421087394,
0.));
#2694=CARTESIAN_POINT('Origin',(0.,0.612722715486149,0.));
#2695=CARTESIAN_POINT('',(-0.6175,0.68,-7.5621939847349E-17));
#2696=CARTESIAN_POINT('Origin',(0.,0.68,0.));
#2697=CARTESIAN_POINT('',(-0.750555349946514,0.603180457891261,-9.19165206894919E-17));
#2698=CARTESIAN_POINT('',(-0.734027674973257,0.612722715486149,-8.98924642641573E-17));
#2699=CARTESIAN_POINT('',(-0.375277674973257,0.603180457891261,0.65));
#2700=CARTESIAN_POINT('Ctrl Pts',(-0.375277674973257,0.603180457891261,
0.65));
#2701=CARTESIAN_POINT('Ctrl Pts',(-0.562916512459968,0.711513791224243,
0.324999999999856));
#2702=CARTESIAN_POINT('Ctrl Pts',(-0.750555349946514,0.603180457891261,
-9.19165206894919E-17));
#2703=CARTESIAN_POINT('',(0.375277674973257,0.603180457891261,0.65));
#2704=CARTESIAN_POINT('Ctrl Pts',(0.375277674973257,0.603180457891261,0.65));
#2705=CARTESIAN_POINT('Ctrl Pts',(-1.66755498298699E-13,0.711513791224244,
0.65));
#2706=CARTESIAN_POINT('Ctrl Pts',(-0.375277674973257,0.603180457891261,
0.65));
#2707=CARTESIAN_POINT('',(0.750555349946514,0.603180457891261,0.));
#2708=CARTESIAN_POINT('Ctrl Pts',(0.750555349946514,0.603180457891261,0.));
#2709=CARTESIAN_POINT('Ctrl Pts',(0.562916512459802,0.711513791224244,0.325000000000144));
#2710=CARTESIAN_POINT('Ctrl Pts',(0.375277674973257,0.603180457891261,0.65));
#2711=CARTESIAN_POINT('',(0.375277674973257,0.603180457891261,-0.65));
#2712=CARTESIAN_POINT('Ctrl Pts',(0.375277674973257,0.603180457891261,-0.65));
#2713=CARTESIAN_POINT('Ctrl Pts',(0.562916512459969,0.711513791224244,-0.324999999999856));
#2714=CARTESIAN_POINT('Ctrl Pts',(0.750555349946514,0.603180457891261,0.));
#2715=CARTESIAN_POINT('',(-0.375277674973257,0.603180457891261,-0.65));
#2716=CARTESIAN_POINT('Ctrl Pts',(-0.375277674973257,0.603180457891261,
-0.65));
#2717=CARTESIAN_POINT('Ctrl Pts',(1.66422431391311E-13,0.711513791224244,
-0.65));
#2718=CARTESIAN_POINT('Ctrl Pts',(0.375277674973257,0.603180457891261,-0.65));
#2719=CARTESIAN_POINT('Ctrl Pts',(-0.750555349946514,0.603180457891261,
-9.19165206894919E-17));
#2720=CARTESIAN_POINT('Ctrl Pts',(-0.562916512459802,0.711513791224244,
-0.325000000000144));
#2721=CARTESIAN_POINT('Ctrl Pts',(-0.375277674973257,0.603180457891261,
-0.65));
#2722=CARTESIAN_POINT('Origin',(0.375277674973257,0.,-0.65));
#2723=CARTESIAN_POINT('',(-0.375277674973257,0.,-0.65));
#2724=CARTESIAN_POINT('',(0.375277674973257,0.,-0.65));
#2725=CARTESIAN_POINT('Origin',(-0.375277674973257,0.,-0.65));
#2726=CARTESIAN_POINT('',(-0.750555349946514,0.,-9.19165206894919E-17));
#2727=CARTESIAN_POINT('Origin',(-0.750555349946514,0.,-9.19165206894919E-17));
#2728=CARTESIAN_POINT('',(-0.375277674973257,0.,0.65));
#2729=CARTESIAN_POINT('Origin',(0.,0.,0.));
#2730=CARTESIAN_POINT('',(-0.338975,0.68,4.15124648740974E-17));
#2731=CARTESIAN_POINT('Origin',(0.,0.68,0.));
#2732=CARTESIAN_POINT('',(-0.338975,0.,4.15124648740974E-17));
#2733=CARTESIAN_POINT('',(-0.338975,0.,4.15124648740974E-17));
#2734=CARTESIAN_POINT('Origin',(0.,0.,0.));
#2735=CARTESIAN_POINT('Origin',(-0.375277674973257,0.,0.65));
#2736=CARTESIAN_POINT('',(0.375277674973257,0.,0.65));
#2737=CARTESIAN_POINT('Origin',(0.750555349946514,0.,0.));
#2738=CARTESIAN_POINT('',(0.750555349946514,0.,0.));
#2739=CARTESIAN_POINT('Origin',(0.375277674973257,0.,0.65));
#2740=CARTESIAN_POINT('Origin',(0.,0.68,-1.11022302462516E-16));
#2741=CARTESIAN_POINT('Origin',(0.,0.,-1.11022302462516E-16));
#2758=UNCERTAINTY_MEASURE_WITH_UNIT(LENGTH_MEASURE(0.001),#2769,
'DISTANCE_ACCURACY_VALUE',
'Maximum model space distance between geometric entities at asserted c
onnectivities');
#2759=UNCERTAINTY_MEASURE_WITH_UNIT(LENGTH_MEASURE(0.001),#2769,
'DISTANCE_ACCURACY_VALUE',
'Maximum model space distance between geometric entities at asserted c
onnectivities');
#2767=(
GEOMETRIC_REPRESENTATION_CONTEXT(3)
GLOBAL_UNCERTAINTY_ASSIGNED_CONTEXT((#2758))
GLOBAL_UNIT_ASSIGNED_CONTEXT((#2769,#2771,#2772))
REPRESENTATION_CONTEXT('','3D')
);
#2768=(
GEOMETRIC_REPRESENTATION_CONTEXT(3)
GLOBAL_UNCERTAINTY_ASSIGNED_CONTEXT((#2759))
GLOBAL_UNIT_ASSIGNED_CONTEXT((#2769,#2771,#2772))
REPRESENTATION_CONTEXT('','3D')
);
#2769=(
LENGTH_UNIT()
NAMED_UNIT(*)
SI_UNIT(.CENTI.,.METRE.)
);
#2771=(
NAMED_UNIT(*)
PLANE_ANGLE_UNIT()
SI_UNIT($,.RADIAN.)
);
#2772=(
NAMED_UNIT(*)
SI_UNIT($,.STERADIAN.)
SOLID_ANGLE_UNIT()
);
#2780=SHAPE_DEFINITION_REPRESENTATION(#2788,#2805);
#2788=PRODUCT_DEFINITION_SHAPE('',$,#2814);
#2805=SHAPE_REPRESENTATION('',(#1812),#2767);
#2806=PRODUCT_DEFINITION_CONTEXT('part definition',#2832,'design');
#2814=PRODUCT_DEFINITION('Hex Nut - M8','Hex Nut - M8',#2822,
#2806);
#2822=PRODUCT_DEFINITION_FORMATION('',$,#2841);
#2832=APPLICATION_CONTEXT(
'Core Data for Automotive Mechanical Design Process');
#2833=PRODUCT_CONTEXT('part definition',#2832,'mechanical');
#2841=PRODUCT('Hex Nut - M8','Hex Nut - M8','Hex Nut - M8',
(#2833));
#2912=COLOUR_RGB('Black',0.12,0.14,0.17);
#2913=FILL_AREA_STYLE_COLOUR('',#2912);
#2914=FILL_AREA_STYLE('',(#2913));
#2915=SURFACE_STYLE_FILL_AREA(#2914);
#2916=SURFACE_SIDE_STYLE('',(#2915));
#2917=SURFACE_STYLE_USAGE(.BOTH.,#2916);
#2918=PRESENTATION_STYLE_ASSIGNMENT((#2917));
ENDSEC;
END-ISO-10303-21;
